ISO-10303-21;
HEADER;
/* Generated by software containing ST-Developer
 * from STEP Tools, Inc. (www.steptools.com) 
 */

FILE_DESCRIPTION(
/* description */ ('Independent manual two-gate roller-track escapement for nominal30mm d
iameter20mm wide feed rollers. Opposed gates are driven by native capt
ured pin-slot loops with positive curved-slot travel stops at\X\B116de
g. Repeated gate/pin/washer/clip instances, adapted native common bear
ing families, full retaining lips and rotating polymer grip. External 
workpieces, gravity feeder/incline and mount anchors outside assembly.
 No powered-feed compatibility, impact, capacity, safety, force, wear 
or life rating.'),
/* implementation_level */ '2;1');

FILE_NAME(
/* name */ 'Pivot thrust washer.step',
/* time_stamp */ '2026-11-08T18:43:23-08:00',
/* author */ (''),
/* organization */ (''),
/* preprocessor_version */ 'ST-DEVELOPER v20.2',
/* originating_system */ 'Autodesk Translation Framework v15.17.0.0',
/* authorisation */ '');

FILE_SCHEMA (('AUTOMOTIVE_DESIGN { 1 0 10303 214 3 1 1 }'));
ENDSEC;

DATA;
#10=MECHANICAL_DESIGN_GEOMETRIC_PRESENTATION_REPRESENTATION('',(#464),#19863);
#426=SHAPE_REPRESENTATION_RELATIONSHIP('SRR','None',#19944,#445);
#445=ADVANCED_BREP_SHAPE_REPRESENTATION('',(#483),#19853);
#464=STYLED_ITEM('',(#20043),#483);
#483=MANIFOLD_SOLID_BREP('Body1',#6433);
#846=LINE('',#15890,#1311);
#847=LINE('',#15896,#1312);
#1311=VECTOR('',#8226,4.);
#1312=VECTOR('',#8233,7.);
#1550=CYLINDRICAL_SURFACE('',#6992,4.);
#1551=CYLINDRICAL_SURFACE('',#6995,7.);
#1669=FACE_BOUND('',#2343,.T.);
#1670=FACE_BOUND('',#2345,.T.);
#1929=FACE_OUTER_BOUND('',#2340,.T.);
#1930=FACE_OUTER_BOUND('',#2341,.T.);
#1931=FACE_OUTER_BOUND('',#2342,.T.);
#1932=FACE_OUTER_BOUND('',#2344,.T.);
#2340=EDGE_LOOP('',(#5385,#5386,#5387,#5388));
#2341=EDGE_LOOP('',(#5389,#5390,#5391,#5392));
#2342=EDGE_LOOP('',(#5393));
#2343=EDGE_LOOP('',(#5394));
#2344=EDGE_LOOP('',(#5395));
#2345=EDGE_LOOP('',(#5396));
#2566=CIRCLE('',#6993,4.);
#2567=CIRCLE('',#6994,4.);
#2568=CIRCLE('',#6996,7.);
#2569=CIRCLE('',#6997,7.);
#3040=VERTEX_POINT('',#15887);
#3041=VERTEX_POINT('',#15889);
#3042=VERTEX_POINT('',#15893);
#3043=VERTEX_POINT('',#15895);
#3851=EDGE_CURVE('',#3040,#3040,#2566,.T.);
#3852=EDGE_CURVE('',#3040,#3041,#846,.T.);
#3853=EDGE_CURVE('',#3041,#3041,#2567,.T.);
#3854=EDGE_CURVE('',#3042,#3042,#2568,.T.);
#3855=EDGE_CURVE('',#3042,#3043,#847,.T.);
#3856=EDGE_CURVE('',#3043,#3043,#2569,.T.);
#5385=ORIENTED_EDGE('',*,*,#3851,.F.);
#5386=ORIENTED_EDGE('',*,*,#3852,.T.);
#5387=ORIENTED_EDGE('',*,*,#3853,.T.);
#5388=ORIENTED_EDGE('',*,*,#3852,.F.);
#5389=ORIENTED_EDGE('',*,*,#3854,.F.);
#5390=ORIENTED_EDGE('',*,*,#3855,.T.);
#5391=ORIENTED_EDGE('',*,*,#3856,.T.);
#5392=ORIENTED_EDGE('',*,*,#3855,.F.);
#5393=ORIENTED_EDGE('',*,*,#3854,.T.);
#5394=ORIENTED_EDGE('',*,*,#3851,.T.);
#5395=ORIENTED_EDGE('',*,*,#3856,.F.);
#5396=ORIENTED_EDGE('',*,*,#3853,.F.);
#6022=PLANE('',#6998);
#6023=PLANE('',#6999);
#6308=ADVANCED_FACE('',(#1929),#1550,.F.);
#6309=ADVANCED_FACE('',(#1930),#1551,.T.);
#6310=ADVANCED_FACE('',(#1931,#1669),#6022,.T.);
#6311=ADVANCED_FACE('',(#1932,#1670),#6023,.F.);
#6433=CLOSED_SHELL('',(#6308,#6309,#6310,#6311));
#6991=AXIS2_PLACEMENT_3D('',#15885,#8220,#8221);
#6992=AXIS2_PLACEMENT_3D('',#15886,#8222,#8223);
#6993=AXIS2_PLACEMENT_3D('',#15888,#8224,#8225);
#6994=AXIS2_PLACEMENT_3D('',#15891,#8227,#8228);
#6995=AXIS2_PLACEMENT_3D('',#15892,#8229,#8230);
#6996=AXIS2_PLACEMENT_3D('',#15894,#8231,#8232);
#6997=AXIS2_PLACEMENT_3D('',#15897,#8234,#8235);
#6998=AXIS2_PLACEMENT_3D('',#15898,#8236,#8237);
#6999=AXIS2_PLACEMENT_3D('',#15899,#8238,#8239);
#8220=DIRECTION('axis',(0.,0.,1.));
#8221=DIRECTION('refdir',(1.,0.,0.));
#8222=DIRECTION('center_axis',(0.,0.,1.));
#8223=DIRECTION('ref_axis',(1.,0.,0.));
#8224=DIRECTION('center_axis',(0.,0.,-1.));
#8225=DIRECTION('ref_axis',(1.,0.,0.));
#8226=DIRECTION('',(0.,0.,-1.));
#8227=DIRECTION('center_axis',(0.,0.,-1.));
#8228=DIRECTION('ref_axis',(1.,0.,0.));
#8229=DIRECTION('center_axis',(0.,0.,1.));
#8230=DIRECTION('ref_axis',(1.,0.,0.));
#8231=DIRECTION('center_axis',(0.,0.,1.));
#8232=DIRECTION('ref_axis',(1.,0.,0.));
#8233=DIRECTION('',(0.,0.,-1.));
#8234=DIRECTION('center_axis',(0.,0.,1.));
#8235=DIRECTION('ref_axis',(1.,0.,0.));
#8236=DIRECTION('center_axis',(0.,0.,1.));
#8237=DIRECTION('ref_axis',(1.,0.,0.));
#8238=DIRECTION('center_axis',(0.,0.,1.));
#8239=DIRECTION('ref_axis',(1.,0.,0.));
#15885=CARTESIAN_POINT('',(0.,0.,0.));
#15886=CARTESIAN_POINT('Origin',(0.,0.,0.));
#15887=CARTESIAN_POINT('',(-4.,-4.89858719658941E-16,2.));
#15888=CARTESIAN_POINT('Origin',(0.,0.,2.));
#15889=CARTESIAN_POINT('',(-4.,-4.89858719658941E-16,0.));
#15890=CARTESIAN_POINT('',(-4.,-4.89858719658941E-16,0.));
#15891=CARTESIAN_POINT('Origin',(0.,0.,0.));
#15892=CARTESIAN_POINT('Origin',(0.,0.,0.));
#15893=CARTESIAN_POINT('',(-7.,-8.57252759403147E-16,2.));
#15894=CARTESIAN_POINT('Origin',(0.,0.,2.));
#15895=CARTESIAN_POINT('',(-7.,-8.57252759403147E-16,0.));
#15896=CARTESIAN_POINT('',(-7.,-8.57252759403147E-16,0.));
#15897=CARTESIAN_POINT('Origin',(0.,0.,0.));
#15898=CARTESIAN_POINT('Origin',(0.,0.,2.));
#15899=CARTESIAN_POINT('Origin',(0.,0.,0.));
#19832=UNCERTAINTY_MEASURE_WITH_UNIT(LENGTH_MEASURE(0.01),#19864,
'DISTANCE_ACCURACY_VALUE',
'Maximum model space distance between geometric entities at asserted c
onnectivities');
#19842=UNCERTAINTY_MEASURE_WITH_UNIT(LENGTH_MEASURE(0.01),#19864,
'DISTANCE_ACCURACY_VALUE',
'Maximum model space distance between geometric entities at asserted c
onnectivities');
#19853=(
GEOMETRIC_REPRESENTATION_CONTEXT(3)
GLOBAL_UNCERTAINTY_ASSIGNED_CONTEXT((#19832))
GLOBAL_UNIT_ASSIGNED_CONTEXT((#19864,#19866,#19867))
REPRESENTATION_CONTEXT('','3D')
);
#19863=(
GEOMETRIC_REPRESENTATION_CONTEXT(3)
GLOBAL_UNCERTAINTY_ASSIGNED_CONTEXT((#19842))
GLOBAL_UNIT_ASSIGNED_CONTEXT((#19864,#19866,#19867))
REPRESENTATION_CONTEXT('','3D')
);
#19864=(
LENGTH_UNIT()
NAMED_UNIT(*)
SI_UNIT(.MILLI.,.METRE.)
);
#19866=(
NAMED_UNIT(*)
PLANE_ANGLE_UNIT()
SI_UNIT($,.RADIAN.)
);
#19867=(
NAMED_UNIT(*)
SI_UNIT($,.STERADIAN.)
SOLID_ANGLE_UNIT()
);
#19878=SHAPE_DEFINITION_REPRESENTATION(#19898,#19944);
#19898=PRODUCT_DEFINITION_SHAPE('',$,#19965);
#19944=SHAPE_REPRESENTATION('',(#6991),#19853);
#19954=PRODUCT_DEFINITION_CONTEXT('part definition',#20016,'design');
#19965=PRODUCT_DEFINITION('Pivot thrust washer','Pivot thrust washer',#19985,
#19954);
#19985=PRODUCT_DEFINITION_FORMATION('',$,#20028);
#20016=APPLICATION_CONTEXT(
'Core Data for Automotive Mechanical Design Process');
#20017=PRODUCT_CONTEXT('part definition',#20016,'mechanical');
#20028=PRODUCT('Pivot thrust washer','Pivot thrust washer',$,(#20017));
#20043=PRESENTATION_STYLE_ASSIGNMENT((#20050));
#20050=SURFACE_STYLE_USAGE(.BOTH.,#20057);
#20057=SURFACE_SIDE_STYLE('',(#20064));
#20064=SURFACE_STYLE_FILL_AREA(#20071);
#20071=FILL_AREA_STYLE('Light gray',(#20078));
#20078=FILL_AREA_STYLE_COLOUR('Light gray',#20085);
#20085=COLOUR_RGB('Light gray',0.725490196078431,0.752941176470588,0.792156862745098);
ENDSEC;
END-ISO-10303-21;
